ISO-10303-21;
HEADER;
/* Generated by software containing ST-Developer
 * from STEP Tools, Inc. (www.steptools.com) 
 */

FILE_DESCRIPTION(
/* description */ (''),
/* implementation_level */ '2;1');

FILE_NAME(
/* name */ 'M3_Nut_04 (1).step',
/* time_stamp */ '2026-10-22T15:07:41+06:00',
/* author */ (''),
/* organization */ (''),
/* preprocessor_version */ 'ST-DEVELOPER v20.2',
/* originating_system */ 'Autodesk Translation Framework v15.15.0.0',
/* authorisation */ '');

FILE_SCHEMA (('AUTOMOTIVE_DESIGN { 1 0 10303 214 3 1 1 }'));
ENDSEC;

DATA;
#10=MECHANICAL_DESIGN_GEOMETRIC_PRESENTATION_REPRESENTATION('',(#2891),#19220);
#80=SHAPE_REPRESENTATION_RELATIONSHIP('SRR','None',#19283,#94);
#94=ADVANCED_BREP_SHAPE_REPRESENTATION('',(#108),#19219);
#108=MANIFOLD_SOLID_BREP('M3_Nut_04',#11327);
#624=FACE_BOUND('',#4498,.T.);
#625=FACE_BOUND('',#4500,.T.);
#831=PLANE('',#12706);
#832=PLANE('',#12707);
#833=PLANE('',#12708);
#834=PLANE('',#12709);
#835=PLANE('',#12710);
#836=PLANE('',#12711);
#837=PLANE('',#12712);
#838=PLANE('',#12713);
#1675=LINE('',#19135,#2530);
#1676=LINE('',#19140,#2531);
#1677=LINE('',#19142,#2532);
#1678=LINE('',#19144,#2533);
#1679=LINE('',#19145,#2534);
#1680=LINE('',#19148,#2535);
#1681=LINE('',#19150,#2536);
#1682=LINE('',#19151,#2537);
#1683=LINE('',#19154,#2538);
#1684=LINE('',#19156,#2539);
#1685=LINE('',#19157,#2540);
#1686=LINE('',#19160,#2541);
#1687=LINE('',#19162,#2542);
#1688=LINE('',#19163,#2543);
#1689=LINE('',#19166,#2544);
#1690=LINE('',#19168,#2545);
#1691=LINE('',#19169,#2546);
#1692=LINE('',#19171,#2547);
#1693=LINE('',#19172,#2548);
#2530=VECTOR('',#16008,1.49999999999999);
#2531=VECTOR('',#16013,10.);
#2532=VECTOR('',#16014,10.);
#2533=VECTOR('',#16015,10.);
#2534=VECTOR('',#16016,10.);
#2535=VECTOR('',#16019,10.);
#2536=VECTOR('',#16020,10.);
#2537=VECTOR('',#16021,10.);
#2538=VECTOR('',#16024,10.);
#2539=VECTOR('',#16025,10.);
#2540=VECTOR('',#16026,10.);
#2541=VECTOR('',#16029,10.);
#2542=VECTOR('',#16030,10.);
#2543=VECTOR('',#16031,10.);
#2544=VECTOR('',#16034,10.);
#2545=VECTOR('',#16035,10.);
#2546=VECTOR('',#16036,10.);
#2547=VECTOR('',#16039,10.);
#2548=VECTOR('',#16040,10.);
#2875=CYLINDRICAL_SURFACE('',#12703,1.465);
#2891=STYLED_ITEM('',(#19410),#108);
#3429=FACE_OUTER_BOUND('',#4490,.T.);
#3430=FACE_OUTER_BOUND('',#4491,.T.);
#3431=FACE_OUTER_BOUND('',#4492,.T.);
#3432=FACE_OUTER_BOUND('',#4493,.T.);
#3433=FACE_OUTER_BOUND('',#4494,.T.);
#3434=FACE_OUTER_BOUND('',#4495,.T.);
#3435=FACE_OUTER_BOUND('',#4496,.T.);
#3436=FACE_OUTER_BOUND('',#4497,.T.);
#3437=FACE_OUTER_BOUND('',#4499,.T.);
#4490=EDGE_LOOP('',(#10720,#10721,#10722,#10723));
#4491=EDGE_LOOP('',(#10724,#10725,#10726,#10727));
#4492=EDGE_LOOP('',(#10728,#10729,#10730,#10731));
#4493=EDGE_LOOP('',(#10732,#10733,#10734,#10735));
#4494=EDGE_LOOP('',(#10736,#10737,#10738,#10739));
#4495=EDGE_LOOP('',(#10740,#10741,#10742,#10743));
#4496=EDGE_LOOP('',(#10744,#10745,#10746,#10747));
#4497=EDGE_LOOP('',(#10748,#10749,#10750,#10751,#10752,#10753));
#4498=EDGE_LOOP('',(#10754));
#4499=EDGE_LOOP('',(#10755,#10756,#10757,#10758,#10759,#10760));
#4500=EDGE_LOOP('',(#10761));
#5169=CIRCLE('',#12704,1.465);
#5170=CIRCLE('',#12705,1.465);
#6173=VERTEX_POINT('',#19132);
#6174=VERTEX_POINT('',#19134);
#6175=VERTEX_POINT('',#19138);
#6176=VERTEX_POINT('',#19139);
#6177=VERTEX_POINT('',#19141);
#6178=VERTEX_POINT('',#19143);
#6179=VERTEX_POINT('',#19147);
#6180=VERTEX_POINT('',#19149);
#6181=VERTEX_POINT('',#19153);
#6182=VERTEX_POINT('',#19155);
#6183=VERTEX_POINT('',#19159);
#6184=VERTEX_POINT('',#19161);
#6185=VERTEX_POINT('',#19165);
#6186=VERTEX_POINT('',#19167);
#7691=EDGE_CURVE('',#6173,#6173,#5169,.T.);
#7692=EDGE_CURVE('',#6173,#6174,#1675,.T.);
#7693=EDGE_CURVE('',#6174,#6174,#5170,.F.);
#7694=EDGE_CURVE('',#6175,#6176,#1676,.T.);
#7695=EDGE_CURVE('',#6175,#6177,#1677,.T.);
#7696=EDGE_CURVE('',#6178,#6177,#1678,.T.);
#7697=EDGE_CURVE('',#6176,#6178,#1679,.T.);
#7698=EDGE_CURVE('',#6176,#6179,#1680,.T.);
#7699=EDGE_CURVE('',#6180,#6178,#1681,.T.);
#7700=EDGE_CURVE('',#6179,#6180,#1682,.T.);
#7701=EDGE_CURVE('',#6179,#6181,#1683,.T.);
#7702=EDGE_CURVE('',#6182,#6180,#1684,.T.);
#7703=EDGE_CURVE('',#6181,#6182,#1685,.T.);
#7704=EDGE_CURVE('',#6181,#6183,#1686,.T.);
#7705=EDGE_CURVE('',#6184,#6182,#1687,.T.);
#7706=EDGE_CURVE('',#6183,#6184,#1688,.T.);
#7707=EDGE_CURVE('',#6183,#6185,#1689,.T.);
#7708=EDGE_CURVE('',#6186,#6184,#1690,.T.);
#7709=EDGE_CURVE('',#6185,#6186,#1691,.T.);
#7710=EDGE_CURVE('',#6185,#6175,#1692,.T.);
#7711=EDGE_CURVE('',#6177,#6186,#1693,.T.);
#10720=ORIENTED_EDGE('',*,*,#7691,.F.);
#10721=ORIENTED_EDGE('',*,*,#7692,.T.);
#10722=ORIENTED_EDGE('',*,*,#7693,.F.);
#10723=ORIENTED_EDGE('',*,*,#7692,.F.);
#10724=ORIENTED_EDGE('',*,*,#7694,.F.);
#10725=ORIENTED_EDGE('',*,*,#7695,.T.);
#10726=ORIENTED_EDGE('',*,*,#7696,.F.);
#10727=ORIENTED_EDGE('',*,*,#7697,.F.);
#10728=ORIENTED_EDGE('',*,*,#7698,.F.);
#10729=ORIENTED_EDGE('',*,*,#7697,.T.);
#10730=ORIENTED_EDGE('',*,*,#7699,.F.);
#10731=ORIENTED_EDGE('',*,*,#7700,.F.);
#10732=ORIENTED_EDGE('',*,*,#7701,.F.);
#10733=ORIENTED_EDGE('',*,*,#7700,.T.);
#10734=ORIENTED_EDGE('',*,*,#7702,.F.);
#10735=ORIENTED_EDGE('',*,*,#7703,.F.);
#10736=ORIENTED_EDGE('',*,*,#7704,.F.);
#10737=ORIENTED_EDGE('',*,*,#7703,.T.);
#10738=ORIENTED_EDGE('',*,*,#7705,.F.);
#10739=ORIENTED_EDGE('',*,*,#7706,.F.);
#10740=ORIENTED_EDGE('',*,*,#7707,.F.);
#10741=ORIENTED_EDGE('',*,*,#7706,.T.);
#10742=ORIENTED_EDGE('',*,*,#7708,.F.);
#10743=ORIENTED_EDGE('',*,*,#7709,.F.);
#10744=ORIENTED_EDGE('',*,*,#7710,.F.);
#10745=ORIENTED_EDGE('',*,*,#7709,.T.);
#10746=ORIENTED_EDGE('',*,*,#7711,.F.);
#10747=ORIENTED_EDGE('',*,*,#7695,.F.);
#10748=ORIENTED_EDGE('',*,*,#7710,.T.);
#10749=ORIENTED_EDGE('',*,*,#7694,.T.);
#10750=ORIENTED_EDGE('',*,*,#7698,.T.);
#10751=ORIENTED_EDGE('',*,*,#7701,.T.);
#10752=ORIENTED_EDGE('',*,*,#7704,.T.);
#10753=ORIENTED_EDGE('',*,*,#7707,.T.);
#10754=ORIENTED_EDGE('',*,*,#7693,.T.);
#10755=ORIENTED_EDGE('',*,*,#7711,.T.);
#10756=ORIENTED_EDGE('',*,*,#7708,.T.);
#10757=ORIENTED_EDGE('',*,*,#7705,.T.);
#10758=ORIENTED_EDGE('',*,*,#7702,.T.);
#10759=ORIENTED_EDGE('',*,*,#7699,.T.);
#10760=ORIENTED_EDGE('',*,*,#7696,.T.);
#10761=ORIENTED_EDGE('',*,*,#7691,.T.);
#11305=ADVANCED_FACE('',(#3429),#2875,.F.);
#11306=ADVANCED_FACE('',(#3430),#831,.T.);
#11307=ADVANCED_FACE('',(#3431),#832,.T.);
#11308=ADVANCED_FACE('',(#3432),#833,.T.);
#11309=ADVANCED_FACE('',(#3433),#834,.T.);
#11310=ADVANCED_FACE('',(#3434),#835,.T.);
#11311=ADVANCED_FACE('',(#3435),#836,.T.);
#11312=ADVANCED_FACE('',(#3436,#624),#837,.T.);
#11313=ADVANCED_FACE('',(#3437,#625),#838,.F.);
#11327=CLOSED_SHELL('',(#11305,#11306,#11307,#11308,#11309,#11310,#11311,
#11312,#11313));
#12702=AXIS2_PLACEMENT_3D('',#19130,#16002,#16003);
#12703=AXIS2_PLACEMENT_3D('',#19131,#16004,#16005);
#12704=AXIS2_PLACEMENT_3D('',#19133,#16006,#16007);
#12705=AXIS2_PLACEMENT_3D('',#19136,#16009,#16010);
#12706=AXIS2_PLACEMENT_3D('',#19137,#16011,#16012);
#12707=AXIS2_PLACEMENT_3D('',#19146,#16017,#16018);
#12708=AXIS2_PLACEMENT_3D('',#19152,#16022,#16023);
#12709=AXIS2_PLACEMENT_3D('',#19158,#16027,#16028);
#12710=AXIS2_PLACEMENT_3D('',#19164,#16032,#16033);
#12711=AXIS2_PLACEMENT_3D('',#19170,#16037,#16038);
#12712=AXIS2_PLACEMENT_3D('',#19173,#16041,#16042);
#12713=AXIS2_PLACEMENT_3D('',#19174,#16043,#16044);
#16002=DIRECTION('axis',(0.,0.,1.));
#16003=DIRECTION('refdir',(1.,0.,0.));
#16004=DIRECTION('center_axis',(0.,-1.,0.));
#16005=DIRECTION('ref_axis',(-1.,0.,0.));
#16006=DIRECTION('center_axis',(0.,1.,0.));
#16007=DIRECTION('ref_axis',(-1.,0.,0.));
#16008=DIRECTION('',(0.,1.,0.));
#16009=DIRECTION('center_axis',(0.,1.,0.));
#16010=DIRECTION('ref_axis',(-1.,0.,0.));
#16011=DIRECTION('center_axis',(-0.866025403784439,0.,-0.499999999999999));
#16012=DIRECTION('ref_axis',(0.499999999999999,0.,-0.866025403784439));
#16013=DIRECTION('',(-0.499999999999999,0.,0.866025403784439));
#16014=DIRECTION('',(0.,-1.,0.));
#16015=DIRECTION('',(0.499999999999999,0.,-0.866025403784439));
#16016=DIRECTION('',(0.,-1.,0.));
#16017=DIRECTION('center_axis',(-0.866025403784439,0.,0.499999999999999));
#16018=DIRECTION('ref_axis',(-0.499999999999999,0.,-0.866025403784439));
#16019=DIRECTION('',(0.499999999999999,0.,0.866025403784439));
#16020=DIRECTION('',(-0.499999999999999,0.,-0.866025403784439));
#16021=DIRECTION('',(0.,-1.,0.));
#16022=DIRECTION('center_axis',(0.,0.,1.));
#16023=DIRECTION('ref_axis',(-1.,0.,0.));
#16024=DIRECTION('',(1.,0.,0.));
#16025=DIRECTION('',(-1.,0.,0.));
#16026=DIRECTION('',(0.,-1.,0.));
#16027=DIRECTION('center_axis',(0.866025403784438,0.,0.500000000000001));
#16028=DIRECTION('ref_axis',(-0.500000000000001,0.,0.866025403784438));
#16029=DIRECTION('',(0.500000000000001,0.,-0.866025403784438));
#16030=DIRECTION('',(-0.500000000000001,0.,0.866025403784438));
#16031=DIRECTION('',(0.,-1.,0.));
#16032=DIRECTION('center_axis',(0.866025403784439,0.,-0.5));
#16033=DIRECTION('ref_axis',(0.5,0.,0.866025403784439));
#16034=DIRECTION('',(-0.5,0.,-0.866025403784439));
#16035=DIRECTION('',(0.5,0.,0.866025403784439));
#16036=DIRECTION('',(0.,-1.,0.));
#16037=DIRECTION('center_axis',(4.61511044732058E-15,0.,-1.));
#16038=DIRECTION('ref_axis',(1.,0.,4.61511044732058E-15));
#16039=DIRECTION('',(-1.,0.,-4.61511044732058E-15));
#16040=DIRECTION('',(1.,0.,4.61511044732058E-15));
#16041=DIRECTION('center_axis',(0.,1.,0.));
#16042=DIRECTION('ref_axis',(-1.,0.,0.));
#16043=DIRECTION('center_axis',(0.,1.,0.));
#16044=DIRECTION('ref_axis',(-1.,0.,0.));
#19130=CARTESIAN_POINT('',(0.,0.,0.));
#19131=CARTESIAN_POINT('Origin',(67.9877341799264,62.5,25.7372649179816));
#19132=CARTESIAN_POINT('',(69.4527341799265,60.5,25.7372649179816));
#19133=CARTESIAN_POINT('Origin',(67.9877341799264,60.5,25.7372649179816));
#19134=CARTESIAN_POINT('',(69.4527341799265,62.5,25.7372649179816));
#19135=CARTESIAN_POINT('',(69.4527341799264,62.5,25.7372649179816));
#19136=CARTESIAN_POINT('Origin',(67.9877341799264,62.5,25.7372649179816));
#19137=CARTESIAN_POINT('Origin',(65.1009828339783,62.5,25.7372649179816));
#19138=CARTESIAN_POINT('',(66.5443585069524,62.5,23.2372649179816));
#19139=CARTESIAN_POINT('',(65.1009828339783,62.5,25.7372649179816));
#19140=CARTESIAN_POINT('',(66.5443585069524,62.5,23.2372649179816));
#19141=CARTESIAN_POINT('',(66.5443585069524,60.5,23.2372649179816));
#19142=CARTESIAN_POINT('',(66.5443585069524,62.5,23.2372649179816));
#19143=CARTESIAN_POINT('',(65.1009828339783,60.5,25.7372649179816));
#19144=CARTESIAN_POINT('',(66.5443585069524,60.5,23.2372649179816));
#19145=CARTESIAN_POINT('',(65.1009828339783,62.5,25.7372649179816));
#19146=CARTESIAN_POINT('Origin',(66.5443585069524,62.5,28.2372649179815));
#19147=CARTESIAN_POINT('',(66.5443585069524,62.5,28.2372649179815));
#19148=CARTESIAN_POINT('',(65.1009828339783,62.5,25.7372649179816));
#19149=CARTESIAN_POINT('',(66.5443585069524,60.5,28.2372649179815));
#19150=CARTESIAN_POINT('',(65.1009828339783,60.5,25.7372649179816));
#19151=CARTESIAN_POINT('',(66.5443585069524,62.5,28.2372649179815));
#19152=CARTESIAN_POINT('Origin',(69.4311098529005,62.5,28.2372649179815));
#19153=CARTESIAN_POINT('',(69.4311098529005,62.5,28.2372649179815));
#19154=CARTESIAN_POINT('',(66.5443585069524,62.5,28.2372649179815));
#19155=CARTESIAN_POINT('',(69.4311098529005,60.5,28.2372649179815));
#19156=CARTESIAN_POINT('',(66.5443585069524,60.5,28.2372649179815));
#19157=CARTESIAN_POINT('',(69.4311098529005,62.5,28.2372649179815));
#19158=CARTESIAN_POINT('Origin',(70.8744855258745,62.5,25.7372649179816));
#19159=CARTESIAN_POINT('',(70.8744855258745,62.5,25.7372649179816));
#19160=CARTESIAN_POINT('',(69.4311098529005,62.5,28.2372649179815));
#19161=CARTESIAN_POINT('',(70.8744855258745,60.5,25.7372649179816));
#19162=CARTESIAN_POINT('',(69.4311098529005,60.5,28.2372649179815));
#19163=CARTESIAN_POINT('',(70.8744855258745,62.5,25.7372649179816));
#19164=CARTESIAN_POINT('Origin',(69.4311098529005,62.5,23.2372649179816));
#19165=CARTESIAN_POINT('',(69.4311098529005,62.5,23.2372649179816));
#19166=CARTESIAN_POINT('',(70.8744855258745,62.5,25.7372649179816));
#19167=CARTESIAN_POINT('',(69.4311098529005,60.5,23.2372649179816));
#19168=CARTESIAN_POINT('',(70.8744855258745,60.5,25.7372649179816));
#19169=CARTESIAN_POINT('',(69.4311098529005,62.5,23.2372649179816));
#19170=CARTESIAN_POINT('Origin',(66.5443585069524,62.5,23.2372649179816));
#19171=CARTESIAN_POINT('',(69.4311098529005,62.5,23.2372649179816));
#19172=CARTESIAN_POINT('',(69.4311098529005,60.5,23.2372649179816));
#19173=CARTESIAN_POINT('Origin',(67.9877341799264,62.5,25.7372649179816));
#19174=CARTESIAN_POINT('Origin',(67.9877341799264,60.5,25.7372649179816));
#19203=UNCERTAINTY_MEASURE_WITH_UNIT(LENGTH_MEASURE(0.01),#19221,
'DISTANCE_ACCURACY_VALUE',
'Maximum model space distance between geometric entities at asserted c
onnectivities');
#19204=UNCERTAINTY_MEASURE_WITH_UNIT(LENGTH_MEASURE(0.01),#19221,
'DISTANCE_ACCURACY_VALUE',
'Maximum model space distance between geometric entities at asserted c
onnectivities');
#19219=(
GEOMETRIC_REPRESENTATION_CONTEXT(3)
GLOBAL_UNCERTAINTY_ASSIGNED_CONTEXT((#19203))
GLOBAL_UNIT_ASSIGNED_CONTEXT((#19221,#19223,#19224))
REPRESENTATION_CONTEXT('','3D')
);
#19220=(
GEOMETRIC_REPRESENTATION_CONTEXT(3)
GLOBAL_UNCERTAINTY_ASSIGNED_CONTEXT((#19204))
GLOBAL_UNIT_ASSIGNED_CONTEXT((#19221,#19223,#19224))
REPRESENTATION_CONTEXT('','3D')
);
#19221=(
LENGTH_UNIT()
NAMED_UNIT(*)
SI_UNIT(.MILLI.,.METRE.)
);
#19223=(
NAMED_UNIT(*)
PLANE_ANGLE_UNIT()
SI_UNIT($,.RADIAN.)
);
#19224=(
NAMED_UNIT(*)
SI_UNIT($,.STERADIAN.)
SOLID_ANGLE_UNIT()
);
#19239=SHAPE_DEFINITION_REPRESENTATION(#19254,#19283);
#19254=PRODUCT_DEFINITION_SHAPE('',$,#19299);
#19283=SHAPE_REPRESENTATION('',(#12702),#19219);
#19284=PRODUCT_DEFINITION_CONTEXT('part definition',#19331,'design');
#19299=PRODUCT_DEFINITION('M3_Nut_04 (1)','M3_Nut_04 (1)',#19314,#19284);
#19314=PRODUCT_DEFINITION_FORMATION('',$,#19347);
#19331=APPLICATION_CONTEXT(
'Core Data for Automotive Mechanical Design Process');
#19332=PRODUCT_CONTEXT('part definition',#19331,'mechanical');
#19347=PRODUCT('M3_Nut_04 (1)','M3_Nut_04 (1)',$,(#19332));
#19404=COLOUR_RGB('Black',0.12,0.14,0.17);
#19405=FILL_AREA_STYLE_COLOUR('',#19404);
#19406=FILL_AREA_STYLE('',(#19405));
#19407=SURFACE_STYLE_FILL_AREA(#19406);
#19408=SURFACE_SIDE_STYLE('',(#19407));
#19409=SURFACE_STYLE_USAGE(.BOTH.,#19408);
#19410=PRESENTATION_STYLE_ASSIGNMENT((#19409));
ENDSEC;
END-ISO-10303-21;
